ISO-10303-21;
HEADER;
/* Generated by software containing ST-Developer
 * from STEP Tools, Inc. (www.steptools.com) 
 */

FILE_DESCRIPTION(
/* description */ ('Turntable on roller ring'),
/* implementation_level */ '2;1');

FILE_NAME(
/* name */ 'Bonded foot (1).step',
/* time_stamp */ '2026-10-28T03:23:59-07:00',
/* author */ (''),
/* organization */ (''),
/* preprocessor_version */ 'ST-DEVELOPER v20.2',
/* originating_system */ 'Autodesk Translation Framework v15.17.0.0',
/* authorisation */ '');

FILE_SCHEMA (('AUTOMOTIVE_DESIGN { 1 0 10303 214 3 1 1 }'));
ENDSEC;

DATA;
#10=MECHANICAL_DESIGN_GEOMETRIC_PRESENTATION_REPRESENTATION('',(#636),#16281);
#517=SHAPE_REPRESENTATION_RELATIONSHIP('SRR','None',#16532,#572);
#572=ADVANCED_BREP_SHAPE_REPRESENTATION('',(#707),#16226);
#636=STYLED_ITEM('',(#16946),#707);
#707=MANIFOLD_SOLID_BREP('Body1',#8378);
#1045=PLANE('',#9382);
#1046=PLANE('',#9383);
#1047=PLANE('',#9384);
#1048=PLANE('',#9385);
#1049=PLANE('',#9386);
#1050=PLANE('',#9387);
#1392=FACE_OUTER_BOUND('',#1973,.T.);
#1393=FACE_OUTER_BOUND('',#1974,.T.);
#1394=FACE_OUTER_BOUND('',#1975,.T.);
#1395=FACE_OUTER_BOUND('',#1976,.T.);
#1396=FACE_OUTER_BOUND('',#1977,.T.);
#1397=FACE_OUTER_BOUND('',#1978,.T.);
#1973=EDGE_LOOP('',(#6269,#6270,#6271,#6272));
#1974=EDGE_LOOP('',(#6273,#6274,#6275,#6276));
#1975=EDGE_LOOP('',(#6277,#6278,#6279,#6280));
#1976=EDGE_LOOP('',(#6281,#6282,#6283,#6284));
#1977=EDGE_LOOP('',(#6285,#6286,#6287,#6288));
#1978=EDGE_LOOP('',(#6289,#6290,#6291,#6292));
#2606=LINE('',#14069,#3089);
#2607=LINE('',#14071,#3090);
#2608=LINE('',#14073,#3091);
#2609=LINE('',#14074,#3092);
#2610=LINE('',#14077,#3093);
#2611=LINE('',#14079,#3094);
#2612=LINE('',#14080,#3095);
#2613=LINE('',#14083,#3096);
#2614=LINE('',#14085,#3097);
#2615=LINE('',#14086,#3098);
#2616=LINE('',#14088,#3099);
#2617=LINE('',#14089,#3100);
#3089=VECTOR('',#10999,1.);
#3090=VECTOR('',#11000,1.);
#3091=VECTOR('',#11001,1.);
#3092=VECTOR('',#11002,1.);
#3093=VECTOR('',#11005,1.);
#3094=VECTOR('',#11006,1.);
#3095=VECTOR('',#11007,1.);
#3096=VECTOR('',#11010,1.);
#3097=VECTOR('',#11011,1.);
#3098=VECTOR('',#11012,1.);
#3099=VECTOR('',#11015,1.);
#3100=VECTOR('',#11016,1.);
#4161=VERTEX_POINT('',#14067);
#4162=VERTEX_POINT('',#14068);
#4163=VERTEX_POINT('',#14070);
#4164=VERTEX_POINT('',#14072);
#4165=VERTEX_POINT('',#14076);
#4166=VERTEX_POINT('',#14078);
#4167=VERTEX_POINT('',#14082);
#4168=VERTEX_POINT('',#14084);
#4945=EDGE_CURVE('',#4161,#4162,#2606,.T.);
#4946=EDGE_CURVE('',#4162,#4163,#2607,.T.);
#4947=EDGE_CURVE('',#4164,#4163,#2608,.T.);
#4948=EDGE_CURVE('',#4161,#4164,#2609,.T.);
#4949=EDGE_CURVE('',#4165,#4161,#2610,.T.);
#4950=EDGE_CURVE('',#4166,#4164,#2611,.T.);
#4951=EDGE_CURVE('',#4165,#4166,#2612,.T.);
#4952=EDGE_CURVE('',#4167,#4165,#2613,.T.);
#4953=EDGE_CURVE('',#4168,#4166,#2614,.T.);
#4954=EDGE_CURVE('',#4167,#4168,#2615,.T.);
#4955=EDGE_CURVE('',#4162,#4167,#2616,.T.);
#4956=EDGE_CURVE('',#4163,#4168,#2617,.T.);
#6269=ORIENTED_EDGE('',*,*,#4945,.T.);
#6270=ORIENTED_EDGE('',*,*,#4946,.T.);
#6271=ORIENTED_EDGE('',*,*,#4947,.F.);
#6272=ORIENTED_EDGE('',*,*,#4948,.F.);
#6273=ORIENTED_EDGE('',*,*,#4949,.T.);
#6274=ORIENTED_EDGE('',*,*,#4948,.T.);
#6275=ORIENTED_EDGE('',*,*,#4950,.F.);
#6276=ORIENTED_EDGE('',*,*,#4951,.F.);
#6277=ORIENTED_EDGE('',*,*,#4952,.T.);
#6278=ORIENTED_EDGE('',*,*,#4951,.T.);
#6279=ORIENTED_EDGE('',*,*,#4953,.F.);
#6280=ORIENTED_EDGE('',*,*,#4954,.F.);
#6281=ORIENTED_EDGE('',*,*,#4955,.T.);
#6282=ORIENTED_EDGE('',*,*,#4954,.T.);
#6283=ORIENTED_EDGE('',*,*,#4956,.F.);
#6284=ORIENTED_EDGE('',*,*,#4946,.F.);
#6285=ORIENTED_EDGE('',*,*,#4956,.T.);
#6286=ORIENTED_EDGE('',*,*,#4953,.T.);
#6287=ORIENTED_EDGE('',*,*,#4950,.T.);
#6288=ORIENTED_EDGE('',*,*,#4947,.T.);
#6289=ORIENTED_EDGE('',*,*,#4955,.F.);
#6290=ORIENTED_EDGE('',*,*,#4945,.F.);
#6291=ORIENTED_EDGE('',*,*,#4949,.F.);
#6292=ORIENTED_EDGE('',*,*,#4952,.F.);
#7995=ADVANCED_FACE('',(#1392),#1045,.T.);
#7996=ADVANCED_FACE('',(#1393),#1046,.T.);
#7997=ADVANCED_FACE('',(#1394),#1047,.T.);
#7998=ADVANCED_FACE('',(#1395),#1048,.T.);
#7999=ADVANCED_FACE('',(#1396),#1049,.T.);
#8000=ADVANCED_FACE('',(#1397),#1050,.F.);
#8378=CLOSED_SHELL('',(#7995,#7996,#7997,#7998,#7999,#8000));
#9381=AXIS2_PLACEMENT_3D('',#14065,#10995,#10996);
#9382=AXIS2_PLACEMENT_3D('',#14066,#10997,#10998);
#9383=AXIS2_PLACEMENT_3D('',#14075,#11003,#11004);
#9384=AXIS2_PLACEMENT_3D('',#14081,#11008,#11009);
#9385=AXIS2_PLACEMENT_3D('',#14087,#11013,#11014);
#9386=AXIS2_PLACEMENT_3D('',#14090,#11017,#11018);
#9387=AXIS2_PLACEMENT_3D('',#14091,#11019,#11020);
#10995=DIRECTION('axis',(0.,0.,1.));
#10996=DIRECTION('refdir',(1.,0.,0.));
#10997=DIRECTION('center_axis',(0.,1.,0.));
#10998=DIRECTION('ref_axis',(-1.,0.,0.));
#10999=DIRECTION('',(-1.,0.,0.));
#11000=DIRECTION('',(0.,0.,1.));
#11001=DIRECTION('',(-1.,0.,0.));
#11002=DIRECTION('',(0.,0.,1.));
#11003=DIRECTION('center_axis',(1.,0.,0.));
#11004=DIRECTION('ref_axis',(0.,1.,0.));
#11005=DIRECTION('',(0.,1.,0.));
#11006=DIRECTION('',(0.,1.,0.));
#11007=DIRECTION('',(0.,0.,1.));
#11008=DIRECTION('center_axis',(0.,-1.,0.));
#11009=DIRECTION('ref_axis',(1.,0.,0.));
#11010=DIRECTION('',(1.,0.,0.));
#11011=DIRECTION('',(1.,0.,0.));
#11012=DIRECTION('',(0.,0.,1.));
#11013=DIRECTION('center_axis',(-1.,0.,0.));
#11014=DIRECTION('ref_axis',(0.,-1.,0.));
#11015=DIRECTION('',(0.,-1.,0.));
#11016=DIRECTION('',(0.,-1.,0.));
#11017=DIRECTION('center_axis',(0.,0.,1.));
#11018=DIRECTION('ref_axis',(1.,0.,0.));
#11019=DIRECTION('center_axis',(0.,0.,1.));
#11020=DIRECTION('ref_axis',(1.,0.,0.));
#14065=CARTESIAN_POINT('',(0.,0.,0.));
#14066=CARTESIAN_POINT('Origin',(20.,21.,-0.6));
#14067=CARTESIAN_POINT('',(20.,21.,-0.6));
#14068=CARTESIAN_POINT('',(18.,21.,-0.6));
#14069=CARTESIAN_POINT('',(20.,21.,-0.6));
#14070=CARTESIAN_POINT('',(18.,21.,0.));
#14071=CARTESIAN_POINT('',(18.,21.,-0.6));
#14072=CARTESIAN_POINT('',(20.,21.,0.));
#14073=CARTESIAN_POINT('',(20.,21.,0.));
#14074=CARTESIAN_POINT('',(20.,21.,-0.6));
#14075=CARTESIAN_POINT('Origin',(20.,-21.,-0.6));
#14076=CARTESIAN_POINT('',(20.,-21.,-0.6));
#14077=CARTESIAN_POINT('',(20.,-21.,-0.6));
#14078=CARTESIAN_POINT('',(20.,-21.,0.));
#14079=CARTESIAN_POINT('',(20.,-21.,0.));
#14080=CARTESIAN_POINT('',(20.,-21.,-0.6));
#14081=CARTESIAN_POINT('Origin',(18.,-21.,-0.6));
#14082=CARTESIAN_POINT('',(18.,-21.,-0.6));
#14083=CARTESIAN_POINT('',(18.,-21.,-0.6));
#14084=CARTESIAN_POINT('',(18.,-21.,0.));
#14085=CARTESIAN_POINT('',(18.,-21.,0.));
#14086=CARTESIAN_POINT('',(18.,-21.,-0.6));
#14087=CARTESIAN_POINT('Origin',(18.,21.,-0.6));
#14088=CARTESIAN_POINT('',(18.,21.,-0.6));
#14089=CARTESIAN_POINT('',(18.,21.,0.));
#14090=CARTESIAN_POINT('Origin',(19.,0.,0.));
#14091=CARTESIAN_POINT('Origin',(19.,0.,-0.6));
#16157=UNCERTAINTY_MEASURE_WITH_UNIT(LENGTH_MEASURE(0.001),#16282,
'DISTANCE_ACCURACY_VALUE',
'Maximum model space distance between geometric entities at asserted c
onnectivities');
#16212=UNCERTAINTY_MEASURE_WITH_UNIT(LENGTH_MEASURE(0.001),#16282,
'DISTANCE_ACCURACY_VALUE',
'Maximum model space distance between geometric entities at asserted c
onnectivities');
#16226=(
GEOMETRIC_REPRESENTATION_CONTEXT(3)
GLOBAL_UNCERTAINTY_ASSIGNED_CONTEXT((#16157))
GLOBAL_UNIT_ASSIGNED_CONTEXT((#16282,#16284,#16285))
REPRESENTATION_CONTEXT('','3D')
);
#16281=(
GEOMETRIC_REPRESENTATION_CONTEXT(3)
GLOBAL_UNCERTAINTY_ASSIGNED_CONTEXT((#16212))
GLOBAL_UNIT_ASSIGNED_CONTEXT((#16282,#16284,#16285))
REPRESENTATION_CONTEXT('','3D')
);
#16282=(
LENGTH_UNIT()
NAMED_UNIT(*)
SI_UNIT(.CENTI.,.METRE.)
);
#16284=(
NAMED_UNIT(*)
PLANE_ANGLE_UNIT()
SI_UNIT($,.RADIAN.)
);
#16285=(
NAMED_UNIT(*)
SI_UNIT($,.STERADIAN.)
SOLID_ANGLE_UNIT()
);
#16299=SHAPE_DEFINITION_REPRESENTATION(#16372,#16532);
#16372=PRODUCT_DEFINITION_SHAPE('',$,#16601);
#16532=SHAPE_REPRESENTATION('',(#9381),#16226);
#16587=PRODUCT_DEFINITION_CONTEXT('part definition',#16793,'design');
#16601=PRODUCT_DEFINITION('Bonded foot (1)','Bonded foot (1)',#16669,#16587);
#16669=PRODUCT_DEFINITION_FORMATION('',$,#16808);
#16793=APPLICATION_CONTEXT(
'Core Data for Automotive Mechanical Design Process');
#16794=PRODUCT_CONTEXT('part definition',#16793,'mechanical');
#16808=PRODUCT('Bonded foot (1)','Bonded foot (1)','Bonded foot (1)',(#16794));
#16940=COLOUR_RGB('Off White',0.89,0.88,0.83);
#16941=FILL_AREA_STYLE_COLOUR('',#16940);
#16942=FILL_AREA_STYLE('',(#16941));
#16943=SURFACE_STYLE_FILL_AREA(#16942);
#16944=SURFACE_SIDE_STYLE('',(#16943));
#16945=SURFACE_STYLE_USAGE(.BOTH.,#16944);
#16946=PRESENTATION_STYLE_ASSIGNMENT((#16945));
ENDSEC;
END-ISO-10303-21;
